ISO-10303-21;
HEADER;
FILE_DESCRIPTION (('STEP AP214'),
    '1' );
FILE_NAME ('o-rings series g_iso_O-ring 23.6x1.8-B-ISO 3601-1.step',
    '2026-09-24T10:28:59',
    ( '' ),
    ( '' ),
    'SwSTEP 2.0',
    'SolidWorks 2026',
    '' );
FILE_SCHEMA (( 'AUTOMOTIVE_DESIGN' ));
ENDSEC;

DATA;
#55=CARTESIAN_POINT ( 'NONE',  ( 0.000000000000000000, 0.000000000000000000, 0.000000000000000000 ) ) ;
#66=ORIENTED_EDGE ( 'NONE', *, *, #7774, .T. ) ;
#279=UNCERTAINTY_MEASURE_WITH_UNIT (LENGTH_MEASURE( 1.000000000000000082E-05 ), #1494, 'distance_accuracy_value', 'NONE');
#447=SHAPE_REPRESENTATION_RELATIONSHIP ( 'NONE' , 'NONE' ,  #12009, #11756 ) ;
#475=VERTEX_POINT ( 'NONE', #2002 ) ;
#698=EDGE_CURVE ( 'NONE', #6225, #6735, #15073, .T. ) ;
#896=EDGE_LOOP ( 'NONE', ( #11196, #11197, #11319, #5052 ) ) ;
#1107=DIRECTION ( 'NONE',  ( -1.000000000000000000, 0.000000000000000000, 0.000000000000000000 ) ) ;
#1113=CIRCLE ( 'NONE', #16478, 13.60000000000000320 ) ;
#1271=SURFACE_STYLE_USAGE ( .BOTH. , #17804 ) ;
#1289=DIRECTION ( 'NONE',  ( -1.000000000000000000, 0.000000000000000000, 0.000000000000000000 ) ) ;
#1445=PRODUCT_DEFINITION_SHAPE ( 'NONE', 'NONE',  #15789 ) ;
#1494=( LENGTH_UNIT ( ) NAMED_UNIT ( * ) SI_UNIT ( .MILLI., .METRE. ) );
#1582=ORIENTED_EDGE ( 'NONE', *, *, #8350, .F. ) ;
#1602=FACE_OUTER_BOUND ( 'NONE', #14479, .T. ) ;
#1784=DIRECTION ( 'NONE',  ( -1.000000000000000000, 0.000000000000000000, 0.000000000000000000 ) ) ;
#1812=( LENGTH_UNIT ( ) NAMED_UNIT ( * ) SI_UNIT ( .MILLI., .METRE. ) );
#2002=CARTESIAN_POINT ( 'NONE',  ( 13.60000000000000320, 1.665519646840400618E-15, 0.000000000000000000 ) ) ;
#2077=COLOUR_RGB ( '', 0.08235294, 0.09019608, 0.10196078) ;
#2283=ORIENTED_EDGE ( 'NONE', *, *, #13061, .T. ) ;
#2316=TOROIDAL_SURFACE ( 'NONE', #17676, 12.70000000000000284, 0.9000000000000003553 ) ;
#2358=ADVANCED_FACE ( 'NONE', ( #8315 ), #3253, .T. ) ;
#2365=MECHANICAL_DESIGN_GEOMETRIC_PRESENTATION_REPRESENTATION('',(#17736),#15665);
#2584=EDGE_CURVE ( 'NONE', #3798, #6225, #14837, .T. ) ;
#2624=( NAMED_UNIT ( * ) SI_UNIT ( $, .STERADIAN. ) SOLID_ANGLE_UNIT ( ) );
#2663=CIRCLE ( 'NONE', #4971, 0.9000000000000003553 ) ;
#2758=ADVANCED_FACE ( 'NONE', ( #11129 ), #4407, .T. ) ;
#2914=CARTESIAN_POINT ( 'NONE',  ( -12.70000000000000284, 0.000000000000000000, 0.000000000000000000 ) ) ;
#2977=APPLICATION_CONTEXT ( 'automotive_design' ) ;
#2983=( NAMED_UNIT ( * ) SI_UNIT ( $, .STERADIAN. ) SOLID_ANGLE_UNIT ( ) );
#3095=ADVANCED_FACE ( 'NONE', ( #14847 ), #5726, .T. ) ;
#3153=( NAMED_UNIT ( * ) PLANE_ANGLE_UNIT ( ) SI_UNIT ( $, .RADIAN. ) );
#3253=TOROIDAL_SURFACE ( 'NONE', #12514, 12.70000000000000284, 0.9000000000000003553 ) ;
#3549=ORIENTED_EDGE ( 'NONE', *, *, #698, .F. ) ;
#3575=AXIS2_PLACEMENT_3D ( 'NONE', #5095, #17575, #9272 ) ;
#3625=EDGE_LOOP ( 'NONE', ( #1582, #7348, #2283, #14185 ) ) ;
#3798=VERTEX_POINT ( 'NONE', #11623 ) ;
#3841=AXIS2_PLACEMENT_3D ( 'NONE', #17376, #9177, #1107 ) ;
#3866=EDGE_CURVE ( 'NONE', #3798, #475, #10324, .T. ) ;
#3892=CARTESIAN_POINT ( 'NONE',  ( 0.000000000000000000, 0.000000000000000000, 0.000000000000000000 ) ) ;
#4085=UNCERTAINTY_MEASURE_WITH_UNIT (LENGTH_MEASURE( 1.000000000000000082E-05 ), #10847, 'distance_accuracy_value', 'NONE');
#4352=( GEOMETRIC_REPRESENTATION_CONTEXT ( 3 ) GLOBAL_UNCERTAINTY_ASSIGNED_CONTEXT ( ( #279 ) ) GLOBAL_UNIT_ASSIGNED_CONTEXT ( ( #1494, #5731, #9806 ) ) REPRESENTATION_CONTEXT ( 'NONE', 'WORKASPACE' ) );
#4371=ORIENTED_EDGE ( 'NONE', *, *, #14666, .F. ) ;
#4407=TOROIDAL_SURFACE ( 'NONE', #16565, 12.70000000000000284, 0.9000000000000003553 ) ;
#4509=CARTESIAN_POINT ( 'NONE',  ( -11.80000000000000249, 0.000000000000000000, 1.102182119232619020E-16 ) ) ;
#4563=DIRECTION ( 'NONE',  ( -0.000000000000000000, -0.000000000000000000, -1.000000000000000000 ) ) ;
#4722=ORIENTED_EDGE ( 'NONE', *, *, #2584, .T. ) ;
#4971=AXIS2_PLACEMENT_3D ( 'NONE', #17742, #14972, #12260 ) ;
#5046=DIRECTION ( 'NONE',  ( -0.000000000000000000, -0.000000000000000000, -1.000000000000000000 ) ) ;
#5052=ORIENTED_EDGE ( 'NONE', *, *, #7774, .F. ) ;
#5095=CARTESIAN_POINT ( 'NONE',  ( 0.000000000000000000, 0.000000000000000000, 0.000000000000000000 ) ) ;
#5128=DIRECTION ( 'NONE',  ( -1.000000000000000000, 0.000000000000000000, 0.000000000000000000 ) ) ;
#5216=CARTESIAN_POINT ( 'NONE',  ( 0.000000000000000000, 0.000000000000000000, 0.000000000000000000 ) ) ;
#5411=( NAMED_UNIT ( * ) PLANE_ANGLE_UNIT ( ) SI_UNIT ( $, .RADIAN. ) );
#5642=SURFACE_STYLE_USAGE ( .BOTH. , #16725 ) ;
#5696=PRODUCT_DEFINITION_FORMATION_WITH_SPECIFIED_SOURCE ( 'ANY', '', #8095, .NOT_KNOWN. ) ;
#5710=DIRECTION ( 'NONE',  ( 0.000000000000000000, 0.000000000000000000, -1.000000000000000000 ) ) ;
#5726=TOROIDAL_SURFACE ( 'NONE', #13566, 12.70000000000000284, 0.9000000000000003553 ) ;
#5731=( NAMED_UNIT ( * ) PLANE_ANGLE_UNIT ( ) SI_UNIT ( $, .RADIAN. ) );
#5782=CIRCLE ( 'NONE', #10120, 11.80000000000000249 ) ;
#5858=CIRCLE ( 'NONE', #11948, 0.8999999999999998002 ) ;
#5958=EDGE_CURVE ( 'NONE', #6735, #475, #1113, .T. ) ;
#6082=COLOUR_RGB ( '', 0.08235294, 0.09019608, 0.10196078) ;
#6222=CARTESIAN_POINT ( 'NONE',  ( 12.70000000000000284, 1.555301434917138827E-15, 0.000000000000000000 ) ) ;
#6225=VERTEX_POINT ( 'NONE', #4509 ) ;
#6545=CARTESIAN_POINT ( 'NONE',  ( 0.000000000000000000, 0.000000000000000000, 0.000000000000000000 ) ) ;
#6735=VERTEX_POINT ( 'NONE', #8165 ) ;
#7092=DIRECTION ( 'NONE',  ( -1.000000000000000000, 0.000000000000000000, 0.000000000000000000 ) ) ;
#7132=DIRECTION ( 'NONE',  ( -0.000000000000000000, -0.000000000000000000, -1.000000000000000000 ) ) ;
#7304=CARTESIAN_POINT ( 'NONE',  ( 0.000000000000000000, 0.000000000000000000, 1.102182119232618281E-16 ) ) ;
#7348=ORIENTED_EDGE ( 'NONE', *, *, #14666, .T. ) ;
#7774=EDGE_CURVE ( 'NONE', #6225, #3798, #5782, .T. ) ;
#7974=DIRECTION ( 'NONE',  ( -0.000000000000000000, -0.000000000000000000, -1.000000000000000000 ) ) ;
#8095=PRODUCT ( 'o-rings series g_iso_O-ring 23.6x1.8-B-ISO 3601-1', 'o-rings series g_iso_O-ring 23.6x1.8-B-ISO 3601-1', '', ( #17018 ) ) ;
#8165=CARTESIAN_POINT ( 'NONE',  ( -13.60000000000000320, 0.000000000000000000, 0.000000000000000000 ) ) ;
#8175=DIRECTION ( 'NONE',  ( -0.000000000000000000, -0.000000000000000000, -1.000000000000000000 ) ) ;
#8187=ORIENTED_EDGE ( 'NONE', *, *, #3866, .F. ) ;
#8315=FACE_OUTER_BOUND ( 'NONE', #896, .T. ) ;
#8350=EDGE_CURVE ( 'NONE', #475, #3798, #5858, .T. ) ;
#8437=DIRECTION ( 'NONE',  ( -0.000000000000000000, -0.000000000000000000, -1.000000000000000000 ) ) ;
#8535=CARTESIAN_POINT ( 'NONE',  ( 12.70000000000000284, 1.555301434917138827E-15, 0.000000000000000000 ) ) ;
#9177=DIRECTION ( 'NONE',  ( -0.000000000000000000, -0.000000000000000000, -1.000000000000000000 ) ) ;
#9272=DIRECTION ( 'NONE',  ( 1.000000000000000000, 0.000000000000000000, 0.000000000000000000 ) ) ;
#9411=SURFACE_STYLE_FILL_AREA ( #16335 ) ;
#9806=( NAMED_UNIT ( * ) SI_UNIT ( $, .STERADIAN. ) SOLID_ANGLE_UNIT ( ) );
#9907=DIRECTION ( 'NONE',  ( -1.000000000000000000, 0.000000000000000000, 0.000000000000000000 ) ) ;
#9989=PRESENTATION_STYLE_ASSIGNMENT (( #5642 ) ) ;
#10120=AXIS2_PLACEMENT_3D ( 'NONE', #7304, #4563, #9907 ) ;
#10132=CLOSED_SHELL ( 'NONE', ( #3095, #2358, #2758, #13772 ) ) ;
#10324=CIRCLE ( 'NONE', #17323, 0.8999999999999998002 ) ;
#10426=STYLED_ITEM ( 'NONE', ( #9989 ), #11551 ) ;
#10716=( GEOMETRIC_REPRESENTATION_CONTEXT ( 3 ) GLOBAL_UNCERTAINTY_ASSIGNED_CONTEXT ( ( #4085 ) ) GLOBAL_UNIT_ASSIGNED_CONTEXT ( ( #10847, #5411, #2624 ) ) REPRESENTATION_CONTEXT ( 'NONE', 'WORKASPACE' ) );
#10798=DIRECTION ( 'NONE',  ( -1.000000000000000000, -1.224646799147353454E-16, 0.000000000000000000 ) ) ;
#10847=( LENGTH_UNIT ( ) NAMED_UNIT ( * ) SI_UNIT ( .MILLI., .METRE. ) );
#11129=FACE_OUTER_BOUND ( 'NONE', #12308, .T. ) ;
#11153=FILL_AREA_STYLE ('',( #12633 ) ) ;
#11196=ORIENTED_EDGE ( 'NONE', *, *, #13061, .F. ) ;
#11197=ORIENTED_EDGE ( 'NONE', *, *, #5958, .T. ) ;
#11319=ORIENTED_EDGE ( 'NONE', *, *, #8350, .T. ) ;
#11438=SURFACE_STYLE_FILL_AREA ( #11153 ) ;
#11551=MANIFOLD_SOLID_BREP ( 'Sweep1', #10132 ) ;
#11623=CARTESIAN_POINT ( 'NONE',  ( 11.80000000000000249, 1.445083222993877036E-15, 0.000000000000000000 ) ) ;
#11756=ADVANCED_BREP_SHAPE_REPRESENTATION ( '', ( #11551, #3575 ), #10716 ) ;
#11881=MECHANICAL_DESIGN_GEOMETRIC_PRESENTATION_REPRESENTATION('',(#10426),#4352);
#11948=AXIS2_PLACEMENT_3D ( 'NONE', #6222, #17511, #14587 ) ;
#12009=SHAPE_REPRESENTATION ( 'o-rings series g_iso_O-ring 23.6x1.8-B-ISO 3601-1', ( #3575 ), #10716 ) ;
#12059=CIRCLE ( 'NONE', #14397, 13.60000000000000320 ) ;
#12260=DIRECTION ( 'NONE',  ( 0.000000000000000000, 0.000000000000000000, -1.000000000000000000 ) ) ;
#12308=EDGE_LOOP ( 'NONE', ( #14157, #3549, #66, #17870 ) ) ;
#12315=DIRECTION ( 'NONE',  ( -1.000000000000000000, 0.000000000000000000, 0.000000000000000000 ) ) ;
#12514=AXIS2_PLACEMENT_3D ( 'NONE', #3892, #7974, #12315 ) ;
#12633=FILL_AREA_STYLE_COLOUR ( '', #6082 ) ;
#13061=EDGE_CURVE ( 'NONE', #6735, #6225, #2663, .T. ) ;
#13566=AXIS2_PLACEMENT_3D ( 'NONE', #5216, #5046, #5128 ) ;
#13772=ADVANCED_FACE ( 'NONE', ( #1602 ), #2316, .T. ) ;
#13792=CARTESIAN_POINT ( 'NONE',  ( 0.000000000000000000, 0.000000000000000000, 0.000000000000000000 ) ) ;
#13972=DIRECTION ( 'NONE',  ( -0.000000000000000000, -0.000000000000000000, -1.000000000000000000 ) ) ;
#14157=ORIENTED_EDGE ( 'NONE', *, *, #5958, .F. ) ;
#14185=ORIENTED_EDGE ( 'NONE', *, *, #2584, .F. ) ;
#14397=AXIS2_PLACEMENT_3D ( 'NONE', #13792, #13972, #7092 ) ;
#14479=EDGE_LOOP ( 'NONE', ( #4371, #8187, #4722, #15977 ) ) ;
#14587=DIRECTION ( 'NONE',  ( -1.000000000000000000, -1.224646799147353454E-16, 0.000000000000000000 ) ) ;
#14666=EDGE_CURVE ( 'NONE', #475, #6735, #12059, .T. ) ;
#14837=CIRCLE ( 'NONE', #3841, 11.80000000000000249 ) ;
#14847=FACE_OUTER_BOUND ( 'NONE', #3625, .T. ) ;
#14971=DIRECTION ( 'NONE',  ( -1.000000000000000000, 0.000000000000000000, 0.000000000000000000 ) ) ;
#14972=DIRECTION ( 'NONE',  ( 0.000000000000000000, -1.000000000000000000, 0.000000000000000000 ) ) ;
#15073=CIRCLE ( 'NONE', #17436, 0.9000000000000003553 ) ;
#15665=( GEOMETRIC_REPRESENTATION_CONTEXT ( 3 ) GLOBAL_UNCERTAINTY_ASSIGNED_CONTEXT ( ( #17345 ) ) GLOBAL_UNIT_ASSIGNED_CONTEXT ( ( #1812, #3153, #2983 ) ) REPRESENTATION_CONTEXT ( 'NONE', 'WORKASPACE' ) );
#15789=PRODUCT_DEFINITION ( 'UNKNOWN', '', #5696, #15872 ) ;
#15872=PRODUCT_DEFINITION_CONTEXT ( 'detailed design', #2977, 'design' ) ;
#15977=ORIENTED_EDGE ( 'NONE', *, *, #698, .T. ) ;
#16335=FILL_AREA_STYLE ('',( #16414 ) ) ;
#16414=FILL_AREA_STYLE_COLOUR ( '', #2077 ) ;
#16436=CARTESIAN_POINT ( 'NONE',  ( 0.000000000000000000, 0.000000000000000000, 0.000000000000000000 ) ) ;
#16478=AXIS2_PLACEMENT_3D ( 'NONE', #6545, #8175, #1289 ) ;
#16565=AXIS2_PLACEMENT_3D ( 'NONE', #16436, #8437, #14971 ) ;
#16618=DIRECTION ( 'NONE',  ( 0.000000000000000000, -1.000000000000000000, 0.000000000000000000 ) ) ;
#16725=SURFACE_SIDE_STYLE ('',( #11438 ) ) ;
#16834=SHAPE_DEFINITION_REPRESENTATION ( #1445, #12009 ) ;
#17018=PRODUCT_CONTEXT ( 'NONE', #17356, 'mechanical' ) ;
#17323=AXIS2_PLACEMENT_3D ( 'NONE', #8535, #17398, #10798 ) ;
#17345=UNCERTAINTY_MEASURE_WITH_UNIT (LENGTH_MEASURE( 1.000000000000000082E-05 ), #1812, 'distance_accuracy_value', 'NONE');
#17356=APPLICATION_CONTEXT ( 'automotive_design' ) ;
#17376=CARTESIAN_POINT ( 'NONE',  ( 0.000000000000000000, 0.000000000000000000, 1.102182119232618281E-16 ) ) ;
#17398=DIRECTION ( 'NONE',  ( -1.224646799147353207E-16, 1.000000000000000000, 0.000000000000000000 ) ) ;
#17436=AXIS2_PLACEMENT_3D ( 'NONE', #2914, #16618, #5710 ) ;
#17511=DIRECTION ( 'NONE',  ( -1.224646799147353207E-16, 1.000000000000000000, 0.000000000000000000 ) ) ;
#17575=DIRECTION ( 'NONE',  ( 0.000000000000000000, 0.000000000000000000, 1.000000000000000000 ) ) ;
#17676=AXIS2_PLACEMENT_3D ( 'NONE', #55, #7132, #1784 ) ;
#17736=STYLED_ITEM ( 'NONE', ( #17885 ), #11756 ) ;
#17742=CARTESIAN_POINT ( 'NONE',  ( -12.70000000000000284, 0.000000000000000000, 0.000000000000000000 ) ) ;
#17804=SURFACE_SIDE_STYLE ('',( #9411 ) ) ;
#17870=ORIENTED_EDGE ( 'NONE', *, *, #3866, .T. ) ;
#17885=PRESENTATION_STYLE_ASSIGNMENT (( #1271 ) ) ;
ENDSEC;
END-ISO-10303-21;
